ISO-10303-21;
HEADER;
FILE_DESCRIPTION (('STEP AP203'),
    '1' );
FILE_NAME ('1602p_c_46.step',
    '2026-10-31T14:11:27',
    ( '' ),
    ( '' ),
    'SwSTEP 2.0',
    'SolidWorks 2024',
    '' );
FILE_SCHEMA (( 'AUTOMOTIVE_DESIGN' ));
ENDSEC;

DATA;
#126=DIRECTION ( 'NONE',  ( 3.837966487416234409E-32, -1.216195237911450118E-15, -1.000000000000000000 ) ) ;
#184=VERTEX_POINT ( 'NONE', #1903 ) ;
#233=AXIS2_PLACEMENT_3D ( 'NONE', #18438, #5592, #126 ) ;
#415=DIRECTION ( 'NONE',  ( 1.000000000000000000, 0.000000000000000000, 0.000000000000000000 ) ) ;
#624=DIRECTION ( 'NONE',  ( 0.2306359803922030383, 0.9730401042858035643, -1.407521210652539229E-17 ) ) ;
#870=AXIS2_PLACEMENT_3D ( 'NONE', #14772, #9688, #624 ) ;
#1464=MANIFOLD_SOLID_BREP ( 'Imported1', #19014 ) ;
#1723=EDGE_LOOP ( 'NONE', ( #6665, #14228, #3502, #23115 ) ) ;
#1735=SHAPE_REPRESENTATION ( '1602p_c_46', ( #12739 ), #15185 ) ;
#1903=CARTESIAN_POINT ( 'NONE',  ( 59.82545934899435025, -8.814969416697280735, 9.256279155971832418E-15 ) ) ;
#2060=CARTESIAN_POINT ( 'NONE',  ( 62.70840910389689782, 3.348031886875279639, 1.061114750357439988E-14 ) ) ;
#2247=EDGE_LOOP ( 'NONE', ( #15108, #11964, #12244, #10519 ) ) ;
#2442=FACE_OUTER_BOUND ( 'NONE', #2247, .T. ) ;
#2569=CARTESIAN_POINT ( 'NONE',  ( 0.000000000000000000, 0.000000000000000000, 0.000000000000000000 ) ) ;
#2573=LINE ( 'NONE', #9830, #4320 ) ;
#2910=EDGE_LOOP ( 'NONE', ( #18021, #13966 ) ) ;
#2914=APPLICATION_CONTEXT ( 'configuration controlled 3d designs of mechanical parts and assemblies' ) ;
#3145=VERTEX_POINT ( 'NONE', #17917 ) ;
#3463=PRODUCT_DEFINITION_FORMATION_WITH_SPECIFIED_SOURCE ( 'ANY', '', #10241, .NOT_KNOWN. ) ;
#3502=ORIENTED_EDGE ( 'NONE', *, *, #20721, .T. ) ;
#3738=CARTESIAN_POINT ( 'NONE',  ( 62.70840910389689782, 3.348031886875279639, 1.061114750357439988E-14 ) ) ;
#3911=EDGE_CURVE ( 'NONE', #3145, #184, #5337, .T. ) ;
#3955=UNCERTAINTY_MEASURE_WITH_UNIT (LENGTH_MEASURE( 1.000000000000000082E-05 ), #5062, 'distance_accuracy_value', 'NONE');
#4265=( NAMED_UNIT ( * ) PLANE_ANGLE_UNIT ( ) SI_UNIT ( $, .RADIAN. ) );
#4320=VECTOR ( 'NONE', #4587, 999.9999999999998863 ) ;
#4486=DIRECTION ( 'NONE',  ( 0.2306359803922032325, 0.9730401042858035643, -1.407521210652540462E-17 ) ) ;
#4587=DIRECTION ( 'NONE',  ( -0.9730401042858036753, 0.2306359803922028995, -2.804983810440358801E-16 ) ) ;
#5062=( LENGTH_UNIT ( ) NAMED_UNIT ( * ) SI_UNIT ( .MILLI., .METRE. ) );
#5286=DIRECTION ( 'NONE',  ( 0.9730401042858036753, -0.2306359803922031493, 2.804983810440361760E-16 ) ) ;
#5337=CIRCLE ( 'NONE', #10358, 12.49999999999999467 ) ;
#5509=DIRECTION ( 'NONE',  ( 0.9730401042858036753, -0.2306359803922031493, 2.804983810440361760E-16 ) ) ;
#5526=EDGE_LOOP ( 'NONE', ( #5886, #22770 ) ) ;
#5592=DIRECTION ( 'NONE',  ( 0.9730401042858035643, -0.2306359803922028717, 2.804983810440357815E-16 ) ) ;
#5659=CARTESIAN_POINT ( 'NONE',  ( 69.48351927594264055, 14.58848926887901065, 1.155720087641903136E-14 ) ) ;
#5886=ORIENTED_EDGE ( 'NONE', *, *, #3911, .F. ) ;
#6039=( NAMED_UNIT ( * ) SI_UNIT ( $, .STERADIAN. ) SOLID_ANGLE_UNIT ( ) );
#6665=ORIENTED_EDGE ( 'NONE', *, *, #19947, .F. ) ;
#7538=ADVANCED_FACE ( 'NONE', ( #19249 ), #13796, .T. ) ;
#7625=CARTESIAN_POINT ( 'NONE',  ( 69.48351927594264055, 14.58848926887901065, 1.155720087641903136E-14 ) ) ;
#8570=EDGE_CURVE ( 'NONE', #13864, #184, #2573, .T. ) ;
#9688=DIRECTION ( 'NONE',  ( -0.9730401042858035643, 0.2306359803922028717, -2.804983810440358308E-16 ) ) ;
#9749=VECTOR ( 'NONE', #14583, 999.9999999999998863 ) ;
#9830=CARTESIAN_POINT ( 'NONE',  ( 63.71761976613755962, -9.737513338266090557, 1.037827268014797219E-14 ) ) ;
#10241=PRODUCT ( '1602p_c_46', '1602p_c_46', '', ( #13826 ) ) ;
#10358=AXIS2_PLACEMENT_3D ( 'NONE', #3738, #5286, #12547 ) ;
#10519=ORIENTED_EDGE ( 'NONE', *, *, #3911, .T. ) ;
#10663=DIRECTION ( 'NONE',  ( 3.837966487416234409E-32, -1.216195237911450118E-15, -1.000000000000000000 ) ) ;
#10699=ADVANCED_FACE ( 'NONE', ( #2442 ), #13360, .T. ) ;
#10911=CIRCLE ( 'NONE', #12420, 12.49999999999999467 ) ;
#10926=LINE ( 'NONE', #5659, #9749 ) ;
#11195=VERTEX_POINT ( 'NONE', #7625 ) ;
#11498=AXIS2_PLACEMENT_3D ( 'NONE', #17429, #20751, #4486 ) ;
#11503=DIRECTION ( 'NONE',  ( 0.2306359803922032325, 0.9730401042858035643, -1.407521210652540462E-17 ) ) ;
#11926=AXIS2_PLACEMENT_3D ( 'NONE', #19670, #11987, #10663 ) ;
#11964=ORIENTED_EDGE ( 'NONE', *, *, #21995, .F. ) ;
#11987=DIRECTION ( 'NONE',  ( 0.9730401042858035643, -0.2306359803922028717, 2.804983810440357815E-16 ) ) ;
#12089=PRODUCT_DEFINITION ( 'UNKNOWN', '', #3463, #18454 ) ;
#12244=ORIENTED_EDGE ( 'NONE', *, *, #21471, .T. ) ;
#12420=AXIS2_PLACEMENT_3D ( 'NONE', #14679, #14794, #11503 ) ;
#12547=DIRECTION ( 'NONE',  ( 0.2306359803922032325, 0.9730401042858035643, -1.407521210652540462E-17 ) ) ;
#12739=AXIS2_PLACEMENT_3D ( 'NONE', #2569, #13380, #415 ) ;
#13360=CYLINDRICAL_SURFACE ( 'NONE', #21222, 12.50000000000000533 ) ;
#13380=DIRECTION ( 'NONE',  ( 0.000000000000000000, 0.000000000000000000, 1.000000000000000000 ) ) ;
#13479=CARTESIAN_POINT ( 'NONE',  ( 66.60056952104010008, 2.425487965306460048, 1.173314102775059961E-14 ) ) ;
#13743=CIRCLE ( 'NONE', #11498, 12.49999999999999467 ) ;
#13796=CYLINDRICAL_SURFACE ( 'NONE', #870, 12.50000000000000533 ) ;
#13826=MECHANICAL_CONTEXT ( 'NONE', #17938, 'mechanical' ) ;
#13864=VERTEX_POINT ( 'NONE', #19900 ) ;
#13966=ORIENTED_EDGE ( 'NONE', *, *, #19947, .T. ) ;
#14228=ORIENTED_EDGE ( 'NONE', *, *, #8570, .T. ) ;
#14583=DIRECTION ( 'NONE',  ( -0.9730401042858036753, 0.2306359803922028995, -2.804983810440358801E-16 ) ) ;
#14679=CARTESIAN_POINT ( 'NONE',  ( 66.60056952104010008, 2.425487965306460048, 1.173314102775059961E-14 ) ) ;
#14772=CARTESIAN_POINT ( 'NONE',  ( 66.60056952104010008, 2.425487965306460048, 1.173314102775059961E-14 ) ) ;
#14794=DIRECTION ( 'NONE',  ( 0.9730401042858036753, -0.2306359803922031493, 2.804983810440361760E-16 ) ) ;
#15108=ORIENTED_EDGE ( 'NONE', *, *, #8570, .F. ) ;
#15126=DIRECTION ( 'NONE',  ( -0.9730401042858035643, 0.2306359803922028717, -2.804983810440358308E-16 ) ) ;
#15185=( GEOMETRIC_REPRESENTATION_CONTEXT ( 3 ) GLOBAL_UNCERTAINTY_ASSIGNED_CONTEXT ( ( #3955 ) ) GLOBAL_UNIT_ASSIGNED_CONTEXT ( ( #5062, #4265, #6039 ) ) REPRESENTATION_CONTEXT ( 'NONE', 'WORKASPACE' ) );
#17429=CARTESIAN_POINT ( 'NONE',  ( 66.60056952104010008, 2.425487965306460048, 1.173314102775059961E-14 ) ) ;
#17777=PLANE ( 'NONE',  #11926 ) ;
#17917=CARTESIAN_POINT ( 'NONE',  ( 65.59135885879943828, 15.51103319044781870, 1.043520735224289159E-14 ) ) ;
#17938=APPLICATION_CONTEXT ( 'configuration controlled 3d designs of mechanical parts and assemblies' ) ;
#17956=AXIS2_PLACEMENT_3D ( 'NONE', #2060, #5509, #17996 ) ;
#17996=DIRECTION ( 'NONE',  ( 0.2306359803922032325, 0.9730401042858035643, -1.407521210652540462E-17 ) ) ;
#18021=ORIENTED_EDGE ( 'NONE', *, *, #21995, .T. ) ;
#18438=CARTESIAN_POINT ( 'NONE',  ( 66.60056952104010008, 2.425487965306460048, 1.173314102775059961E-14 ) ) ;
#18454=DESIGN_CONTEXT ( 'detailed design', #2914, 'design' ) ;
#18560=ADVANCED_FACE ( 'NONE', ( #19558 ), #17777, .F. ) ;
#19008=ADVANCED_BREP_SHAPE_REPRESENTATION ( '', ( #1464, #12739 ), #15185 ) ;
#19014=CLOSED_SHELL ( 'NONE', ( #7538, #10699, #18560, #21266 ) ) ;
#19249=FACE_OUTER_BOUND ( 'NONE', #1723, .T. ) ;
#19558=FACE_OUTER_BOUND ( 'NONE', #5526, .T. ) ;
#19670=CARTESIAN_POINT ( 'NONE',  ( 62.70840910389689782, 3.348031886875279639, 1.061114750357439988E-14 ) ) ;
#19900=CARTESIAN_POINT ( 'NONE',  ( 63.71761976613755962, -9.737513338266090557, 1.037827268014797219E-14 ) ) ;
#19947=EDGE_CURVE ( 'NONE', #13864, #11195, #13743, .T. ) ;
#20209=PLANE ( 'NONE',  #233 ) ;
#20605=DIRECTION ( 'NONE',  ( 0.2306359803922030383, 0.9730401042858035643, -1.407521210652539229E-17 ) ) ;
#20708=SHAPE_DEFINITION_REPRESENTATION ( #22924, #1735 ) ;
#20721=EDGE_CURVE ( 'NONE', #184, #3145, #22502, .T. ) ;
#20751=DIRECTION ( 'NONE',  ( 0.9730401042858036753, -0.2306359803922031493, 2.804983810440361760E-16 ) ) ;
#20973=SHAPE_REPRESENTATION_RELATIONSHIP ( 'NONE' , 'NONE' ,  #1735, #19008 ) ;
#21222=AXIS2_PLACEMENT_3D ( 'NONE', #13479, #15126, #20605 ) ;
#21266=ADVANCED_FACE ( 'NONE', ( #23400 ), #20209, .T. ) ;
#21471=EDGE_CURVE ( 'NONE', #11195, #3145, #10926, .T. ) ;
#21995=EDGE_CURVE ( 'NONE', #11195, #13864, #10911, .T. ) ;
#22502=CIRCLE ( 'NONE', #17956, 12.49999999999999467 ) ;
#22770=ORIENTED_EDGE ( 'NONE', *, *, #20721, .F. ) ;
#22924=PRODUCT_DEFINITION_SHAPE ( 'NONE', 'NONE',  #12089 ) ;
#23115=ORIENTED_EDGE ( 'NONE', *, *, #21471, .F. ) ;
#23400=FACE_OUTER_BOUND ( 'NONE', #2910, .T. ) ;
#23543=COLOUR_RGB('Light Gray', 0.72549020, 0.75294118, 0.79215686);
#23544=FILL_AREA_STYLE_COLOUR('',#23543);
#23545=FILL_AREA_STYLE('',(#23544));
#23546=SURFACE_STYLE_FILL_AREA(#23545);
#23547=SURFACE_SIDE_STYLE('',(#23546));
#23548=SURFACE_STYLE_USAGE(.BOTH.,#23547);
#23549=PRESENTATION_STYLE_ASSIGNMENT((#23548));
#23621=STYLED_ITEM('',(#23549),#1464);
#23622=MECHANICAL_DESIGN_GEOMETRIC_PRESENTATION_REPRESENTATION('',(#23621),#15185);
ENDSEC;
END-ISO-10303-21;
